ISO-10303-21;
HEADER;
FILE_DESCRIPTION (('STEP AP214'),
    '1' );
FILE_NAME ('hex bolt gradeb_iso_ISO 4015 - M10 x 40 x 26-N.step',
    '2026-10-10T03:43:58',
    ( '' ),
    ( '' ),
    'SwSTEP 2.0',
    'SolidWorks 2026',
    '' );
FILE_SCHEMA (( 'AUTOMOTIVE_DESIGN' ));
ENDSEC;

DATA;
#164=CARTESIAN_POINT ( 'NONE',  ( 46.39999999999999858, 0.000000000000000000, 0.000000000000000000 ) ) ;
#216=AXIS2_PLACEMENT_3D ( 'NONE', #62327, #35605, #30325 ) ;
#270=CARTESIAN_POINT ( 'NONE',  ( 0.06730325657897140434, -1.557442666625558525, -8.000000000000000000 ) ) ;
#294=ORIENTED_EDGE ( 'NONE', *, *, #30490, .T. ) ;
#387=CARTESIAN_POINT ( 'NONE',  ( 0.1317522424472117037, 1.959574484719860621, 8.000000000000000000 ) ) ;
#589=DIRECTION ( 'NONE',  ( 0.000000000000000000, 0.000000000000000000, -1.000000000000000000 ) ) ;
#630=CARTESIAN_POINT ( 'NONE',  ( 0.4973051450695675224, -3.866309095700863896, -8.000000000000000000 ) ) ;
#712=FACE_OUTER_BOUND ( 'NONE', #13803, .T. ) ;
#757=DIRECTION ( 'NONE',  ( -1.000000000000000000, -0.000000000000000000, -0.000000000000000000 ) ) ;
#845=CARTESIAN_POINT ( 'NONE',  ( 0.06809871960543363578, -7.710219529346616696, 2.645508037661887801 ) ) ;
#896=ADVANCED_FACE ( 'NONE', ( #44876 ), #22778, .T. ) ;
#980=CARTESIAN_POINT ( 'NONE',  ( 1.219727444046191995E-16, -0.7818963812181061179, -8.000000000000000000 ) ) ;
#1373=CARTESIAN_POINT ( 'NONE',  ( 0.08285530295198803574, 1.570896314769985702, -8.000000000000000000 ) ) ;
#1432=EDGE_CURVE ( 'NONE', #52541, #47772, #5936, .T. ) ;
#2069=CARTESIAN_POINT ( 'NONE',  ( 0.000000000000000000, 0.000000000000000000, 8.000000000000000000 ) ) ;
#2261=DIRECTION ( 'NONE',  ( -0.7071067811865483499, 8.659560562354925463E-17, -0.7071067811865467956 ) ) ;
#2262=UNCERTAINTY_MEASURE_WITH_UNIT (LENGTH_MEASURE( 1.000000000000000082E-05 ), #25461, 'distance_accuracy_value', 'NONE');
#2398=CARTESIAN_POINT ( 'NONE',  ( 6.400000000000000355, -4.618802153517011178, 8.000000000000000000 ) ) ;
#2750=DIRECTION ( 'NONE',  ( 0.000000000000000000, 0.5000000000000009992, 0.8660254037844380415 ) ) ;
#2878=DIRECTION ( 'NONE',  ( 0.000000000000000000, 0.000000000000000000, -1.000000000000000000 ) ) ;
#3030=ORIENTED_EDGE ( 'NONE', *, *, #19041, .F. ) ;
#3075=CARTESIAN_POINT ( 'NONE',  ( 0.000000000000000000, 6.928203230275505220, -4.000000000000007994 ) ) ;
#3084=CIRCLE ( 'NONE', #66010, 5.000000000000000000 ) ;
#3140=APPLICATION_CONTEXT ( 'automotive_design' ) ;
#3477=CARTESIAN_POINT ( 'NONE',  ( 0.7145311798163274108, 9.237604307034018802, -2.124379920709345337E-16 ) ) ;
#3675=CARTESIAN_POINT ( 'NONE',  ( 6.400000000000000355, 4.618802153517001408, -8.000000000000000000 ) ) ;
#3754=EDGE_CURVE ( 'NONE', #4587, #18030, #61352, .T. ) ;
#3825=CARTESIAN_POINT ( 'NONE',  ( 0.000000000000000000, 6.928203230275506108, 4.000000000000006217 ) ) ;
#3860=ADVANCED_BREP_SHAPE_REPRESENTATION ( '', ( #63623, #66832 ), #10752 ) ;
#3896=ORIENTED_EDGE ( 'NONE', *, *, #60752, .F. ) ;
#4039=SURFACE_STYLE_FILL_AREA ( #30775 ) ;
#4065=EDGE_LOOP ( 'NONE', ( #60343, #16016, #47481, #9262 ) ) ;
#4097=PRODUCT_DEFINITION_FORMATION_WITH_SPECIFIED_SOURCE ( 'ANY', '', #62996, .NOT_KNOWN. ) ;
#4587=VERTEX_POINT ( 'NONE', #12222 ) ;
#4595=VECTOR ( 'NONE', #8965, 1000.000000000000000 ) ;
#4766=FACE_OUTER_BOUND ( 'NONE', #24856, .T. ) ;
#4943=AXIS2_PLACEMENT_3D ( 'NONE', #56175, #41396, #7991 ) ;
#5032=DIRECTION ( 'NONE',  ( -0.000000000000000000, 0.000000000000000000, -1.000000000000000000 ) ) ;
#5190=CARTESIAN_POINT ( 'NONE',  ( 0.000000000000000000, 0.000000000000000000, 0.000000000000000000 ) ) ;
#5224=AXIS2_PLACEMENT_3D ( 'NONE', #67576, #45774, #40485 ) ;
#5294=CARTESIAN_POINT ( 'NONE',  ( 6.400000000000000355, -4.618802153517016507, -8.000000000000000000 ) ) ;
#5315=CIRCLE ( 'NONE', #30041, 8.000000000000000000 ) ;
#5331=CARTESIAN_POINT ( 'NONE',  ( 0.01678220609566008145, 0.7854258609844494421, 8.000000000000000000 ) ) ;
#5501=CARTESIAN_POINT ( 'NONE',  ( 0.000000000000000000, -6.928203230275505220, -4.000000000000007105 ) ) ;
#5619=ADVANCED_FACE ( 'NONE', ( #24182 ), #19228, .F. ) ;
#5936=CIRCLE ( 'NONE', #53086, 8.000000000000000000 ) ;
#6186=DIRECTION ( 'NONE',  ( 0.000000000000000000, -1.000000000000000000, 0.000000000000000000 ) ) ;
#6401=PRODUCT_DEFINITION_CONTEXT ( 'detailed design', #3140, 'design' ) ;
#6581=CARTESIAN_POINT ( 'NONE',  ( 6.400000000000000355, 9.237604307034018802, 0.000000000000000000 ) ) ;
#6629=CARTESIAN_POINT ( 'NONE',  ( 6.400000000000000355, 9.237604307034018802, 0.000000000000000000 ) ) ;
#6780=CIRCLE ( 'NONE', #216, 4.171999999999999709 ) ;
#6963=CLOSED_SHELL ( 'NONE', ( #60211, #67512, #40431, #9371, #67043, #24788, #37880, #33756, #65184, #28841, #896, #68548, #35695, #21448, #68969, #49345, #68203, #15940, #5619 ) ) ;
#7369=ORIENTED_EDGE ( 'NONE', *, *, #50014, .F. ) ;
#7379=CARTESIAN_POINT ( 'NONE',  ( 0.7145311798163228589, 4.618802153517005848, 8.000000000000000000 ) ) ;
#7544=VERTEX_POINT ( 'NONE', #32920 ) ;
#7744=B_SPLINE_CURVE_WITH_KNOTS ( 'NONE', 3,
 ( #19448, #56051, #68921, #34949, #24048, #9856 ),
 .UNSPECIFIED., .F., .F.,
 ( 4, 2, 4 ),
 ( 0.008690415895085791889, 0.01102883710845594875, 0.01336725832182610388 ),
 .UNSPECIFIED. ) ;
#7768=ORIENTED_EDGE ( 'NONE', *, *, #47234, .T. ) ;
#7882=UNCERTAINTY_MEASURE_WITH_UNIT (LENGTH_MEASURE( 1.000000000000000082E-05 ), #14926, 'distance_accuracy_value', 'NONE');
#7921=ORIENTED_EDGE ( 'NONE', *, *, #53261, .T. ) ;
#7991=DIRECTION ( 'NONE',  ( -0.000000000000000000, 0.000000000000000000, -1.000000000000000000 ) ) ;
#8020=ORIENTED_EDGE ( 'NONE', *, *, #29314, .F. ) ;
#8132=CARTESIAN_POINT ( 'NONE',  ( 0.1306530452038078272, 5.952467836904149934, -5.690023276062396107 ) ) ;
#8133=LINE ( 'NONE', #18689, #26336 ) ;
#8233=SHAPE_REPRESENTATION_RELATIONSHIP ( 'NONE' , 'NONE' ,  #60409, #3860 ) ;
#8254=DIRECTION ( 'NONE',  ( 0.000000000000000000, 0.000000000000000000, -1.000000000000000000 ) ) ;
#8319=DIRECTION ( 'NONE',  ( 1.000000000000000000, 0.000000000000000000, 0.000000000000000000 ) ) ;
#8341=EDGE_CURVE ( 'NONE', #61856, #4587, #54589, .T. ) ;
#8649=CARTESIAN_POINT ( 'NONE',  ( 0.000000000000000000, 0.000000000000000000, 0.000000000000000000 ) ) ;
#8691=CARTESIAN_POINT ( 'NONE',  ( 0.000000000000000000, 0.000000000000000000, 0.000000000000000000 ) ) ;
#8840=FACE_OUTER_BOUND ( 'NONE', #4065, .T. ) ;
#8907=EDGE_CURVE ( 'NONE', #56288, #17657, #66059, .T. ) ;
#8965=DIRECTION ( 'NONE',  ( -1.000000000000000000, -0.000000000000000000, -0.000000000000000000 ) ) ;
#9032=DIRECTION ( 'NONE',  ( 1.000000000000000000, 0.000000000000000000, -0.000000000000000000 ) ) ;
#9178=VECTOR ( 'NONE', #30636, 1000.000000000000000 ) ;
#9262=ORIENTED_EDGE ( 'NONE', *, *, #30490, .F. ) ;
#9371=ADVANCED_FACE ( 'NONE', ( #9485 ), #63644, .F. ) ;
#9485=FACE_OUTER_BOUND ( 'NONE', #40553, .T. ) ;
#9856=CARTESIAN_POINT ( 'NONE',  ( 0.000000000000000000, 0.000000000000000000, 8.000000000000000000 ) ) ;
#9919=ORIENTED_EDGE ( 'NONE', *, *, #8341, .T. ) ;
#10042=DIRECTION ( 'NONE',  ( 0.000000000000000000, 0.000000000000000000, 1.000000000000000000 ) ) ;
#10244=ORIENTED_EDGE ( 'NONE', *, *, #49853, .F. ) ;
#10386=EDGE_CURVE ( 'NONE', #62269, #16032, #69255, .T. ) ;
#10481=CARTESIAN_POINT ( 'NONE',  ( 0.3157512944565323831, -3.097794232830194172, -8.000000000000000000 ) ) ;
#10562=DIRECTION ( 'NONE',  ( 0.000000000000000000, -0.5000000000000008882, 0.8660254037844381525 ) ) ;
#10675=SURFACE_SIDE_STYLE ('',( #4039 ) ) ;
#10752=( GEOMETRIC_REPRESENTATION_CONTEXT ( 3 ) GLOBAL_UNCERTAINTY_ASSIGNED_CONTEXT ( ( #2262 ) ) GLOBAL_UNIT_ASSIGNED_CONTEXT ( ( #25461, #51498, #13512 ) ) REPRESENTATION_CONTEXT ( 'NONE', 'WORKASPACE' ) );
#10852=AXIS2_PLACEMENT_3D ( 'NONE', #30942, #36562, #68567 ) ;
#10883=DIRECTION ( 'NONE',  ( 0.000000000000000000, 0.000000000000000000, -1.000000000000000000 ) ) ;
#10891=VECTOR ( 'NONE', #15405, 1000.000000000000000 ) ;
#10917=B_SPLINE_CURVE_WITH_KNOTS ( 'NONE', 3,
 ( #49541, #60103, #33397, #11925, #1373, #20484, #54468, #52832 ),
 .UNSPECIFIED., .F., .F.,
 ( 4, 2, 2, 4 ),
 ( 0.02285338877108900393, 0.02519297479642216772, 0.02636276780908874962, 0.02753256082175533151 ),
 .UNSPECIFIED. ) ;
#11339=CARTESIAN_POINT ( 'NONE',  ( 6.400000000000000355, 9.237604307034018802, 0.000000000000000000 ) ) ;
#11380=CARTESIAN_POINT ( 'NONE',  ( 0.3167204509598451900, -8.479269695850872424, 1.313474075707216748 ) ) ;
#11574=CARTESIAN_POINT ( 'NONE',  ( 6.400000000000000355, 6.123233995736766282E-16, -5.000000000000000000 ) ) ;
#11708=AXIS2_PLACEMENT_3D ( 'NONE', #29359, #36020, #8254 ) ;
#11733=ORIENTED_EDGE ( 'NONE', *, *, #52690, .F. ) ;
#11925=CARTESIAN_POINT ( 'NONE',  ( 0.1317522424472107878, 1.959574484719855736, -8.000000000000000000 ) ) ;
#12017=CARTESIAN_POINT ( 'NONE',  ( 0.000000000000000000, 6.928203230275505220, -4.000000000000007994 ) ) ;
#12030=EDGE_LOOP ( 'NONE', ( #60262, #3030, #68455, #32444, #32513 ) ) ;
#12201=CARTESIAN_POINT ( 'NONE',  ( 6.400000000000000355, 4.618802153517001408, -8.000000000000000000 ) ) ;
#12222=CARTESIAN_POINT ( 'NONE',  ( 46.39999999999999858, 0.000000000000000000, 4.171999999999999709 ) ) ;
#12230=CARTESIAN_POINT ( 'NONE',  ( 6.400000000000000355, -4.618802153517016507, -8.000000000000000000 ) ) ;
#12239=EDGE_LOOP ( 'NONE', ( #21012, #18495, #11733, #34173 ) ) ;
#12715=CARTESIAN_POINT ( 'NONE',  ( -3.973643313806734888E-15, 6.732211846623391338, -4.339467034331192075 ) ) ;
#12886=FACE_OUTER_BOUND ( 'NONE', #67029, .T. ) ;
#12903=CARTESIAN_POINT ( 'NONE',  ( 6.400000000000000355, 4.618802153517001408, -8.000000000000000000 ) ) ;
#13284=MECHANICAL_DESIGN_GEOMETRIC_PRESENTATION_REPRESENTATION('',(#63832),#66066);
#13423=ORIENTED_EDGE ( 'NONE', *, *, #47234, .F. ) ;
#13512=( NAMED_UNIT ( * ) SI_UNIT ( $, .STERADIAN. ) SOLID_ANGLE_UNIT ( ) );
#13803=EDGE_LOOP ( 'NONE', ( #55434, #8020, #7369, #49703, #48341 ) ) ;
#13885=EDGE_CURVE ( 'NONE', #64675, #48379, #23173, .T. ) ;
#13999=DIRECTION ( 'NONE',  ( 0.000000000000000000, 0.000000000000000000, -1.000000000000000000 ) ) ;
#14173=DIRECTION ( 'NONE',  ( 0.000000000000000000, 0.000000000000000000, 1.000000000000000000 ) ) ;
#14322=ORIENTED_EDGE ( 'NONE', *, *, #20983, .F. ) ;
#14514=CARTESIAN_POINT ( 'NONE',  ( 0.000000000000000000, 0.000000000000000000, 0.000000000000000000 ) ) ;
#14775=EDGE_CURVE ( 'NONE', #17657, #20172, #10917, .T. ) ;
#14865=PLANE ( 'NONE',  #58902 ) ;
#14926=( LENGTH_UNIT ( ) NAMED_UNIT ( * ) SI_UNIT ( .MILLI., .METRE. ) );
#15057=DIRECTION ( 'NONE',  ( 1.000000000000000000, 0.000000000000000000, -0.000000000000000000 ) ) ;
#15233=CARTESIAN_POINT ( 'NONE',  ( 0.08224679563972019103, -7.710515798486379246, -2.644994884459114459 ) ) ;
#15296=B_SPLINE_CURVE_WITH_KNOTS ( 'NONE', 3,
 ( #58472, #31415, #63426, #15233, #37362, #26134, #36003, #36698 ),
 .UNSPECIFIED., .F., .F.,
 ( 4, 2, 2, 4 ),
 ( 0.004673709593152144438, 0.005837709341827637330, 0.007001709090503131089, 0.009329708587854116872 ),
 .UNSPECIFIED. ) ;
#15405=DIRECTION ( 'NONE',  ( -1.000000000000000000, -0.000000000000000000, -0.000000000000000000 ) ) ;
#15417=CARTESIAN_POINT ( 'NONE',  ( 0.4969600502617522730, 8.860760056385746708, 0.6527133886630306359 ) ) ;
#15766=CARTESIAN_POINT ( 'NONE',  ( 0.000000000000000000, -6.928203230275503444, 4.000000000000010658 ) ) ;
#15783=DIRECTION ( 'NONE',  ( 0.000000000000000000, 0.000000000000000000, -1.000000000000000000 ) ) ;
#15852=EDGE_CURVE ( 'NONE', #52541, #48379, #34375, .T. ) ;
#15940=ADVANCED_FACE ( 'NONE', ( #67809 ), #22578, .T. ) ;
#15987=CARTESIAN_POINT ( 'NONE',  ( 6.400000000000000355, 4.618802153517001408, -8.000000000000000000 ) ) ;
#16016=ORIENTED_EDGE ( 'NONE', *, *, #42397, .T. ) ;
#16032=VERTEX_POINT ( 'NONE', #5501 ) ;
#16352=EDGE_CURVE ( 'NONE', #7544, #65894, #42564, .T. ) ;
#16414=EDGE_CURVE ( 'NONE', #63967, #7544, #28981, .T. ) ;
#16442=LINE ( 'NONE', #38951, #33360 ) ;
#16463=ORIENTED_EDGE ( 'NONE', *, *, #16352, .T. ) ;
#16798=ORIENTED_EDGE ( 'NONE', *, *, #50903, .F. ) ;
#16977=CIRCLE ( 'NONE', #41701, 8.000000000000000000 ) ;
#17227=ORIENTED_EDGE ( 'NONE', *, *, #20983, .T. ) ;
#17444=CARTESIAN_POINT ( 'NONE',  ( 0.000000000000000000, 0.000000000000000000, 0.000000000000000000 ) ) ;
#17657=VERTEX_POINT ( 'NONE', #55985 ) ;
#17755=EDGE_CURVE ( 'NONE', #34426, #55546, #62984, .T. ) ;
#17768=EDGE_LOOP ( 'NONE', ( #60113, #17227, #58862, #42747, #60664, #7768 ) ) ;
#17838=VERTEX_POINT ( 'NONE', #11574 ) ;
#18030=VERTEX_POINT ( 'NONE', #43602 ) ;
#18209=ORIENTED_EDGE ( 'NONE', *, *, #15852, .F. ) ;
#18331=CARTESIAN_POINT ( 'NONE',  ( 0.7145311798163210826, 4.618802153517001408, -8.000000000000000000 ) ) ;
#18396=CARTESIAN_POINT ( 'NONE',  ( 2.307317748320714124E-15, -6.534749472788169200, -4.681481898396984143 ) ) ;
#18409=DIRECTION ( 'NONE',  ( -1.000000000000000000, -0.000000000000000000, -0.000000000000000000 ) ) ;
#18495=ORIENTED_EDGE ( 'NONE', *, *, #29789, .T. ) ;
#18540=EDGE_CURVE ( 'NONE', #65894, #16032, #16977, .T. ) ;
#18689=CARTESIAN_POINT ( 'NONE',  ( 0.000000000000000000, 0.000000000000000000, 5.000000000000000000 ) ) ;
#18711=DIRECTION ( 'NONE',  ( 1.000000000000000000, 0.000000000000000000, 0.000000000000000000 ) ) ;
#18803=EDGE_LOOP ( 'NONE', ( #23315, #46564, #66587 ) ) ;
#18858=EDGE_LOOP ( 'NONE', ( #32028, #53768 ) ) ;
#18889=VERTEX_POINT ( 'NONE', #68041 ) ;
#19041=EDGE_CURVE ( 'NONE', #29324, #65564, #33858, .T. ) ;
#19228=PLANE ( 'NONE',  #4943 ) ;
#19258=DIRECTION ( 'NONE',  ( 1.000000000000000000, 0.000000000000000000, 0.000000000000000000 ) ) ;
#19347=ORIENTED_EDGE ( 'NONE', *, *, #13885, .T. ) ;
#19448=CARTESIAN_POINT ( 'NONE',  ( 0.7145311798163248573, -4.618802153517011178, 8.000000000000000000 ) ) ;
#19549=AXIS2_PLACEMENT_3D ( 'NONE', #15987, #42716, #59574 ) ;
#19874=( NAMED_UNIT ( * ) PLANE_ANGLE_UNIT ( ) SI_UNIT ( $, .RADIAN. ) );
#19923=DIRECTION ( 'NONE',  ( 0.000000000000000000, 0.5000000000000013323, 0.8660254037844379305 ) ) ;
#19944=AXIS2_PLACEMENT_3D ( 'NONE', #66915, #18711, #2878 ) ;
#19986=CARTESIAN_POINT ( 'NONE',  ( 46.39999999999999858, 5.616230220889761452E-16, -4.171999999999999709 ) ) ;
#19992=VECTOR ( 'NONE', #61456, 1000.000000000000000 ) ;
#20172=VERTEX_POINT ( 'NONE', #45377 ) ;
#20266=EDGE_LOOP ( 'NONE', ( #62457, #30578, #48710, #26934 ) ) ;
#20305=DIRECTION ( 'NONE',  ( -1.000000000000000000, -0.000000000000000000, 0.000000000000000000 ) ) ;
#20388=DIRECTION ( 'NONE',  ( -1.000000000000000000, -0.000000000000000000, -0.000000000000000000 ) ) ;
#20453=CARTESIAN_POINT ( 'NONE',  ( 45.57199999999999562, 6.123233995736766282E-16, -5.000000000000000000 ) ) ;
#20484=CARTESIAN_POINT ( 'NONE',  ( 0.01678220609566017166, 0.7854258609844448902, -8.000000000000000000 ) ) ;
#20868=DIRECTION ( 'NONE',  ( 1.000000000000000000, 0.000000000000000000, -0.000000000000000000 ) ) ;
#20948=DIRECTION ( 'NONE',  ( 0.000000000000000000, 0.8660254037844379305, -0.5000000000000013323 ) ) ;
#20966=EDGE_CURVE ( 'NONE', #47585, #29324, #34067, .T. ) ;
#20983=EDGE_CURVE ( 'NONE', #29324, #64675, #44612, .T. ) ;
#21012=ORIENTED_EDGE ( 'NONE', *, *, #66879, .T. ) ;
#21138=PLANE ( 'NONE',  #57516 ) ;
#21448=ADVANCED_FACE ( 'NONE', ( #12886 ), #25091, .T. ) ;
#21610=B_SPLINE_CURVE_WITH_KNOTS ( 'NONE', 3,
 ( #23372, #45851, #39878, #55713, #28995, #45148 ),
 .UNSPECIFIED., .F., .F.,
 ( 4, 2, 4 ),
 ( 2.380731629582122378E-07, 0.002336973833157555101, 0.004673709593152151377 ),
 .UNSPECIFIED. ) ;
#21725=CARTESIAN_POINT ( 'NONE',  ( 2.087089182034596824E-15, -6.732211846623400220, 4.339467034331201845 ) ) ;
#21798=AXIS2_PLACEMENT_3D ( 'NONE', #64701, #48155, #10883 ) ;
#21884=EDGE_CURVE ( 'NONE', #55546, #52541, #7744, .T. ) ;
#21947=AXIS2_PLACEMENT_3D ( 'NONE', #69120, #20948, #19923 ) ;
#21952=ORIENTED_EDGE ( 'NONE', *, *, #19041, .T. ) ;
#22232=ORIENTED_EDGE ( 'NONE', *, *, #21884, .T. ) ;
#22297=CARTESIAN_POINT ( 'NONE',  ( 2.105723906874191037E-15, -7.321656987762880320, 3.318518101603019854 ) ) ;
#22311=CARTESIAN_POINT ( 'NONE',  ( 46.39999999999999858, 5.109226446042757607E-16, -4.171999999999999709 ) ) ;
#22431=VECTOR ( 'NONE', #55876, 1000.000000000000000 ) ;
#22482=ORIENTED_EDGE ( 'NONE', *, *, #1432, .T. ) ;
#22546=CARTESIAN_POINT ( 'NONE',  ( 0.08285530295198817452, 1.570896314769990587, 8.000000000000000000 ) ) ;
#22559=EDGE_CURVE ( 'NONE', #61856, #51247, #60641, .T. ) ;
#22578=CONICAL_SURFACE ( 'NONE', #23748, 8.000000000000000000, 1.047197551196600296 ) ;
#22624=CARTESIAN_POINT ( 'NONE',  ( 0.7145311798163274108, 9.237604307034018802, -2.124379920709345337E-16 ) ) ;
#22778=CONICAL_SURFACE ( 'NONE', #28400, 4.171999999999999709, 0.7853981633974472798 ) ;
#22811=AXIS2_PLACEMENT_3D ( 'NONE', #17444, #44535, #65293 ) ;
#22865=AXIS2_PLACEMENT_3D ( 'NONE', #54552, #757, #43649 ) ;
#22889=ORIENTED_EDGE ( 'NONE', *, *, #25373, .T. ) ;
#22927=DIRECTION ( 'NONE',  ( 0.000000000000000000, 0.000000000000000000, -1.000000000000000000 ) ) ;
#22957=CIRCLE ( 'NONE', #51032, 5.000000000000000000 ) ;
#23173=LINE ( 'NONE', #44618, #22431 ) ;
#23315=ORIENTED_EDGE ( 'NONE', *, *, #8907, .T. ) ;
#23316=VECTOR ( 'NONE', #34362, 1000.000000000000000 ) ;
#23372=CARTESIAN_POINT ( 'NONE',  ( 0.7145311798163228589, 4.618802153517005848, 8.000000000000000000 ) ) ;
#23682=CARTESIAN_POINT ( 'NONE',  ( 0.7145311798161619876, -4.618802153517266085, -8.000000000000000000 ) ) ;
#23748=AXIS2_PLACEMENT_3D ( 'NONE', #28524, #19258, #65826 ) ;
#23844=AXIS2_PLACEMENT_3D ( 'NONE', #50649, #66854, #61558 ) ;
#23959=CARTESIAN_POINT ( 'NONE',  ( 0.3173508448886513400, 5.375634714784618851, -6.689127551062007626 ) ) ;
#24048=CARTESIAN_POINT ( 'NONE',  ( -8.470329472542999693E-17, -0.7818963812180738104, 8.000000000000000000 ) ) ;
#24070=CARTESIAN_POINT ( 'NONE',  ( 46.39999999999999858, 0.000000000000000000, 4.171999999999999709 ) ) ;
#24182=FACE_OUTER_BOUND ( 'NONE', #57636, .T. ) ;
#24371=FACE_OUTER_BOUND ( 'NONE', #48789, .T. ) ;
#24581=LINE ( 'NONE', #34783, #29890 ) ;
#24788=ADVANCED_FACE ( 'NONE', ( #4766 ), #35759, .F. ) ;
#24850=PRODUCT_CONTEXT ( 'NONE', #44409, 'mechanical' ) ;
#24856=EDGE_LOOP ( 'NONE', ( #65849, #56941, #54165, #28596, #55192 ) ) ;
#24939=CARTESIAN_POINT ( 'NONE',  ( 0.3173508448886560029, 8.480771745766405800, 1.310872448937997259 ) ) ;
#25078=B_SPLINE_CURVE_WITH_KNOTS ( 'NONE', 3,
 ( #22624, #50056, #59893, #60261, #55322, #39506 ),
 .UNSPECIFIED., .F., .F.,
 ( 4, 2, 4 ),
 ( 2.380731629581200700E-07, 0.002336973833157563775, 0.004673709593152168724 ),
 .UNSPECIFIED. ) ;
#25091=CONICAL_SURFACE ( 'NONE', #22811, 8.000000000000000000, 1.047197551196600296 ) ;
#25171=ORIENTED_EDGE ( 'NONE', *, *, #3754, .T. ) ;
#25373=EDGE_CURVE ( 'NONE', #52541, #65894, #57911, .T. ) ;
#25376=CARTESIAN_POINT ( 'NONE',  ( 6.400000000000000355, 0.000000000000000000, 0.000000000000000000 ) ) ;
#25461=( LENGTH_UNIT ( ) NAMED_UNIT ( * ) SI_UNIT ( .MILLI., .METRE. ) );
#25779=B_SPLINE_CURVE_WITH_KNOTS ( 'NONE', 3,
 ( #3825, #62919, #31589, #51671, #53028, #24939, #15417, #3477 ),
 .UNSPECIFIED., .F., .F.,
 ( 4, 2, 2, 4 ),
 ( 0.004673709593152151377, 0.005837709341827642534, 0.007001709090503133691, 0.009329708587854115137 ),
 .UNSPECIFIED. ) ;
#25815=FACE_BOUND ( 'NONE', #52151, .T. ) ;
#26134=CARTESIAN_POINT ( 'NONE',  ( 0.3173508448886623312, -8.480771745766416458, -1.310872448937996593 ) ) ;
#26336=VECTOR ( 'NONE', #40479, 1000.000000000000000 ) ;
#26399=DIRECTION ( 'NONE',  ( 0.000000000000000000, 0.000000000000000000, -1.000000000000000000 ) ) ;
#26786=CARTESIAN_POINT ( 'NONE',  ( 0.3194001229790418561, 3.115132258388588760, 8.000000000000001776 ) ) ;
#26934=ORIENTED_EDGE ( 'NONE', *, *, #3754, .F. ) ;
#27289=CARTESIAN_POINT ( 'NONE',  ( 6.400000000000000355, 4.618802153517004960, 8.000000000000000000 ) ) ;
#27697=CARTESIAN_POINT ( 'NONE',  ( 0.01688885742777274449, -6.535341423375596648, 4.680456609903981935 ) ) ;
#27713=DIRECTION ( 'NONE',  ( 0.000000000000000000, 0.000000000000000000, 1.000000000000000000 ) ) ;
#27960=ORIENTED_EDGE ( 'NONE', *, *, #34648, .F. ) ;
#28076=DIRECTION ( 'NONE',  ( 0.000000000000000000, -0.5000000000000007772, 0.8660254037844381525 ) ) ;
#28236=EDGE_CURVE ( 'NONE', #34426, #63967, #24581, .T. ) ;
#28292=DIRECTION ( 'NONE',  ( -0.7071067811865483499, 0.000000000000000000, 0.7071067811865467956 ) ) ;
#28338=CIRCLE ( 'NONE', #54168, 5.000000000000000000 ) ;
#28400=AXIS2_PLACEMENT_3D ( 'NONE', #50153, #61053, #38549 ) ;
#28524=CARTESIAN_POINT ( 'NONE',  ( 0.000000000000000000, 0.000000000000000000, 0.000000000000000000 ) ) ;
#28596=ORIENTED_EDGE ( 'NONE', *, *, #17755, .T. ) ;
#28841=ADVANCED_FACE ( 'NONE', ( #8840 ), #30290, .T. ) ;
#28901=CARTESIAN_POINT ( 'NONE',  ( 0.4969600502617471105, 4.995646404165273502, -7.347286611336972584 ) ) ;
#28981=LINE ( 'NONE', #45138, #42843 ) ;
#28995=CARTESIAN_POINT ( 'NONE',  ( -2.873135757086586750E-15, 6.534749472788147884, 4.681481898397000130 ) ) ;
#29314=EDGE_CURVE ( 'NONE', #59875, #62269, #16442, .T. ) ;
#29316=DIRECTION ( 'NONE',  ( -1.000000000000000000, -0.000000000000000000, -0.000000000000000000 ) ) ;
#29324=VERTEX_POINT ( 'NONE', #6581 ) ;
#29359=CARTESIAN_POINT ( 'NONE',  ( 0.000000000000000000, 0.000000000000000000, 0.000000000000000000 ) ) ;
#29746=DIRECTION ( 'NONE',  ( 1.000000000000000000, 0.000000000000000000, 0.000000000000000000 ) ) ;
#29789=EDGE_CURVE ( 'NONE', #51247, #17838, #52345, .T. ) ;
#29890=VECTOR ( 'NONE', #40050, 1000.000000000000000 ) ;
#30041=AXIS2_PLACEMENT_3D ( 'NONE', #38762, #65853, #22927 ) ;
#30290=CYLINDRICAL_SURFACE ( 'NONE', #5224, 5.000000000000000000 ) ;
#30325=DIRECTION ( 'NONE',  ( 0.000000000000000000, 0.000000000000000000, 1.000000000000000000 ) ) ;
#30490=EDGE_CURVE ( 'NONE', #17838, #18889, #3084, .T. ) ;
#30578=ORIENTED_EDGE ( 'NONE', *, *, #22559, .T. ) ;
#30636=DIRECTION ( 'NONE',  ( -1.000000000000000000, -0.000000000000000000, -0.000000000000000000 ) ) ;
#30775=FILL_AREA_STYLE ('',( #31801 ) ) ;
#30903=ORIENTED_EDGE ( 'NONE', *, *, #15852, .T. ) ;
#30942=CARTESIAN_POINT ( 'NONE',  ( 6.400000000000000355, 9.237604307034018802, 0.000000000000000000 ) ) ;
#31063=DIRECTION ( 'NONE',  ( -1.000000000000000000, 0.000000000000000000, -0.000000000000000000 ) ) ;
#31405=ORIENTED_EDGE ( 'NONE', *, *, #1432, .F. ) ;
#31415=CARTESIAN_POINT ( 'NONE',  ( 2.349104707051926800E-15, -7.124194613927633313, -3.660532965668826133 ) ) ;
#31499=DIRECTION ( 'NONE',  ( -1.000000000000000000, -0.000000000000000000, -0.000000000000000000 ) ) ;
#31558=PRODUCT_DEFINITION_SHAPE ( 'NONE', 'NONE',  #46114 ) ;
#31589=CARTESIAN_POINT ( 'NONE',  ( 0.01688885742776758889, 7.321065037175426227, 3.319543390096036717 ) ) ;
#31801=FILL_AREA_STYLE_COLOUR ( '', #34632 ) ;
#32028=ORIENTED_EDGE ( 'NONE', *, *, #66565, .F. ) ;
#32099=AXIS2_PLACEMENT_3D ( 'NONE', #64118, #58831, #64815 ) ;
#32444=ORIENTED_EDGE ( 'NONE', *, *, #50903, .T. ) ;
#32513=ORIENTED_EDGE ( 'NONE', *, *, #8907, .F. ) ;
#32818=CARTESIAN_POINT ( 'NONE',  ( 0.7145311798161619876, -4.618802153517266085, -8.000000000000000000 ) ) ;
#32920=CARTESIAN_POINT ( 'NONE',  ( 0.7145311798163349604, -9.237604307034033013, 2.857026868940023748E-16 ) ) ;
#32961=DIRECTION ( 'NONE',  ( -1.000000000000000000, -0.000000000000000000, -0.000000000000000000 ) ) ;
#32997=CARTESIAN_POINT ( 'NONE',  ( 45.57199999999999562, 0.000000000000000000, 0.000000000000000000 ) ) ;
#33273=AXIS2_PLACEMENT_3D ( 'NONE', #52736, #20388, #43208 ) ;
#33360=VECTOR ( 'NONE', #32961, 1000.000000000000000 ) ;
#33397=CARTESIAN_POINT ( 'NONE',  ( 0.3194001229790404128, 3.115132258388582542, -8.000000000000000000 ) ) ;
#33756=ADVANCED_FACE ( 'NONE', ( #24371 ), #56719, .F. ) ;
#33858=LINE ( 'NONE', #11339, #58550 ) ;
#34067=LINE ( 'NONE', #55509, #39593 ) ;
#34137=B_SPLINE_CURVE_WITH_KNOTS ( 'NONE', 3,
 ( #15766, #21725, #27697, #64298, #47768, #43175, #42500, #49138 ),
 .UNSPECIFIED., .F., .F.,
 ( 4, 2, 2, 4 ),
 ( 0.004673709593152181735, 0.005837709341827665953, 0.007001709090503150171, 0.009329708587854116872 ),
 .UNSPECIFIED. ) ;
#34173=ORIENTED_EDGE ( 'NONE', *, *, #68780, .F. ) ;
#34185=CONICAL_SURFACE ( 'NONE', #21798, 8.000000000000000000, 1.047197551196600296 ) ;
#34362=DIRECTION ( 'NONE',  ( -0.000000000000000000, 1.000000000000000000, -0.000000000000000000 ) ) ;
#34375=B_SPLINE_CURVE_WITH_KNOTS ( 'NONE', 3,
 ( #58777, #49611, #5331, #22546, #387, #26786, #42612, #37675 ),
 .UNSPECIFIED., .F., .F.,
 ( 4, 2, 2, 4 ),
 ( 0.01336725832182610388, 0.01453745201803767137, 0.01570764571424923886, 0.01804803310667237384 ),
 .UNSPECIFIED. ) ;
#34426=VERTEX_POINT ( 'NONE', #2398 ) ;
#34439=ORIENTED_EDGE ( 'NONE', *, *, #49851, .T. ) ;
#34632=COLOUR_RGB ( '',0.7921568627450980005, 0.8196078431372548767, 0.9333333333333333481 ) ;
#34648=EDGE_CURVE ( 'NONE', #64675, #34426, #61656, .T. ) ;
#34783=CARTESIAN_POINT ( 'NONE',  ( 6.400000000000000355, -9.237604307034033013, -1.753283555911559014E-16 ) ) ;
#34949=CARTESIAN_POINT ( 'NONE',  ( 0.06730325657896543690, -1.557442666625494576, 8.000000000000000000 ) ) ;
#35029=FACE_OUTER_BOUND ( 'NONE', #36607, .T. ) ;
#35176=VECTOR ( 'NONE', #28292, 999.9999999999998863 ) ;
#35401=SHAPE_DEFINITION_REPRESENTATION ( #31558, #60409 ) ;
#35605=DIRECTION ( 'NONE',  ( -1.000000000000000000, -0.000000000000000000, -0.000000000000000000 ) ) ;
#35695=ADVANCED_FACE ( 'NONE', ( #35029 ), #60725, .T. ) ;
#35759=PLANE ( 'NONE',  #21947 ) ;
#36003=CARTESIAN_POINT ( 'NONE',  ( 0.4969600502617602111, -8.860760056385760919, -0.6527133886630297477 ) ) ;
#36020=DIRECTION ( 'NONE',  ( 1.000000000000000000, 0.000000000000000000, -0.000000000000000000 ) ) ;
#36289=ORIENTED_EDGE ( 'NONE', *, *, #18540, .T. ) ;
#36331=CARTESIAN_POINT ( 'NONE',  ( 46.39999999999999858, 0.000000000000000000, 0.000000000000000000 ) ) ;
#36360=CARTESIAN_POINT ( 'NONE',  ( 6.400000000000000355, -7.806255641895631925E-15, -15.99999999999998579 ) ) ;
#36562=DIRECTION ( 'NONE',  ( 0.000000000000000000, -0.8660254037844382635, -0.5000000000000006661 ) ) ;
#36607=EDGE_LOOP ( 'NONE', ( #62323, #59726, #58034 ) ) ;
#36698=CARTESIAN_POINT ( 'NONE',  ( 0.7145311798163349604, -9.237604307034033013, 2.857026868940023748E-16 ) ) ;
#37179=DIRECTION ( 'NONE',  ( 1.000000000000000000, 0.000000000000000000, 0.000000000000000000 ) ) ;
#37229=DIRECTION ( 'NONE',  ( -1.000000000000000000, 0.000000000000000000, -0.000000000000000000 ) ) ;
#37362=CARTESIAN_POINT ( 'NONE',  ( 0.1306530452038165702, -7.903938623646881823, -2.309976723937614107 ) ) ;
#37628=DIRECTION ( 'NONE',  ( -1.000000000000000000, -0.000000000000000000, 0.000000000000000000 ) ) ;
#37675=CARTESIAN_POINT ( 'NONE',  ( 0.7145311798163228589, 4.618802153517005848, 8.000000000000000000 ) ) ;
#37711=CONICAL_SURFACE ( 'NONE', #55702, 4.171999999999999709, 0.7853981633974472798 ) ;
#37880=ADVANCED_FACE ( 'NONE', ( #712 ), #21138, .F. ) ;
#38038=CYLINDRICAL_SURFACE ( 'NONE', #22865, 5.000000000000000000 ) ;
#38219=FACE_OUTER_BOUND ( 'NONE', #58207, .T. ) ;
#38549=DIRECTION ( 'NONE',  ( 0.000000000000000000, 0.000000000000000000, 1.000000000000000000 ) ) ;
#38687=CIRCLE ( 'NONE', #11708, 8.000000000000000000 ) ;
#38762=CARTESIAN_POINT ( 'NONE',  ( 0.000000000000000000, 0.000000000000000000, 0.000000000000000000 ) ) ;
#38951=CARTESIAN_POINT ( 'NONE',  ( 6.400000000000000355, -4.618802153517016507, -8.000000000000000000 ) ) ;
#39506=CARTESIAN_POINT ( 'NONE',  ( 0.000000000000000000, 6.928203230275505220, -4.000000000000007994 ) ) ;
#39555=AXIS2_PLACEMENT_3D ( 'NONE', #42517, #15783, #37229 ) ;
#39593=VECTOR ( 'NONE', #2750, 1000.000000000000114 ) ;
#39719=CARTESIAN_POINT ( 'NONE',  ( 6.400000000000000355, -4.618802153517016507, -8.000000000000000000 ) ) ;
#39792=CARTESIAN_POINT ( 'NONE',  ( 0.01688885742776611437, 6.535341423375590431, -4.680456609903974829 ) ) ;
#39853=CARTESIAN_POINT ( 'NONE',  ( 0.000000000000000000, -6.928203230275505220, -4.000000000000007105 ) ) ;
#39878=CARTESIAN_POINT ( 'NONE',  ( 0.3167204509598370299, 5.377136764700159333, 6.686525924292792133 ) ) ;
#40050=DIRECTION ( 'NONE',  ( -0.000000000000000000, -0.5000000000000013323, -0.8660254037844379305 ) ) ;
#40308=FACE_OUTER_BOUND ( 'NONE', #18858, .T. ) ;
#40431=ADVANCED_FACE ( 'NONE', ( #59234 ), #49370, .F. ) ;
#40479=DIRECTION ( 'NONE',  ( -1.000000000000000000, -0.000000000000000000, -0.000000000000000000 ) ) ;
#40485=DIRECTION ( 'NONE',  ( 0.000000000000000000, 0.000000000000000000, 1.000000000000000000 ) ) ;
#40510=EDGE_CURVE ( 'NONE', #48379, #47772, #21610, .T. ) ;
#40553=EDGE_LOOP ( 'NONE', ( #53801, #56890, #14322, #21952, #3896 ) ) ;
#41260=ORIENTED_EDGE ( 'NONE', *, *, #29314, .T. ) ;
#41396=DIRECTION ( 'NONE',  ( 1.000000000000000000, 0.000000000000000000, -0.000000000000000000 ) ) ;
#41701=AXIS2_PLACEMENT_3D ( 'NONE', #8691, #9032, #46297 ) ;
#42397=EDGE_CURVE ( 'NONE', #51247, #18030, #22957, .T. ) ;
#42500=CARTESIAN_POINT ( 'NONE',  ( 0.4969600502617513293, -4.995646404165285936, 7.347286611336975248 ) ) ;
#42517=CARTESIAN_POINT ( 'NONE',  ( 6.400000000000000355, 4.618802153517004960, 8.000000000000000000 ) ) ;
#42564=B_SPLINE_CURVE_WITH_KNOTS ( 'NONE', 3,
 ( #59223, #48653, #11380, #845, #22297, #44805 ),
 .UNSPECIFIED., .F., .F.,
 ( 4, 2, 4 ),
 ( 2.380731629583756093E-07, 0.002336973833157569413, 0.004673709593152181735 ),
 .UNSPECIFIED. ) ;
#42612=CARTESIAN_POINT ( 'NONE',  ( 0.4988340113715887814, 3.871605243926956152, 8.000000000000001776 ) ) ;
#42716=DIRECTION ( 'NONE',  ( 0.000000000000000000, -0.8660254037844380415, 0.5000000000000009992 ) ) ;
#42747=ORIENTED_EDGE ( 'NONE', *, *, #28236, .T. ) ;
#42826=CARTESIAN_POINT ( 'NONE',  ( 0.7145311798161619876, -4.618802153517266085, -8.000000000000000000 ) ) ;
#42843=VECTOR ( 'NONE', #29316, 1000.000000000000000 ) ;
#43175=CARTESIAN_POINT ( 'NONE',  ( 0.3173508448886570021, -5.375634714784626844, 6.689127551062011179 ) ) ;
#43208=DIRECTION ( 'NONE',  ( 0.000000000000000000, 0.000000000000000000, 1.000000000000000000 ) ) ;
#43298=FACE_OUTER_BOUND ( 'NONE', #12239, .T. ) ;
#43594=ORIENTED_EDGE ( 'NONE', *, *, #21884, .F. ) ;
#43602=CARTESIAN_POINT ( 'NONE',  ( 45.57199999999999562, 0.000000000000000000, 5.000000000000000000 ) ) ;
#43649=DIRECTION ( 'NONE',  ( 0.000000000000000000, 0.000000000000000000, 1.000000000000000000 ) ) ;
#43765=AXIS2_PLACEMENT_3D ( 'NONE', #45815, #68641, #67293 ) ;
#44409=APPLICATION_CONTEXT ( 'automotive_design' ) ;
#44535=DIRECTION ( 'NONE',  ( 1.000000000000000000, 0.000000000000000000, 0.000000000000000000 ) ) ;
#44558=DIRECTION ( 'NONE',  ( 0.000000000000000000, 0.000000000000000000, 1.000000000000000000 ) ) ;
#44612=LINE ( 'NONE', #6629, #48534 ) ;
#44618=CARTESIAN_POINT ( 'NONE',  ( 6.400000000000000355, 4.618802153517004960, 8.000000000000000000 ) ) ;
#44805=CARTESIAN_POINT ( 'NONE',  ( 0.000000000000000000, -6.928203230275503444, 4.000000000000010658 ) ) ;
#44876=FACE_OUTER_BOUND ( 'NONE', #52446, .T. ) ;
#45125=CARTESIAN_POINT ( 'NONE',  ( 0.06809871960542919489, -6.146186931204441706, -5.354491962338086886 ) ) ;
#45138=CARTESIAN_POINT ( 'NONE',  ( 6.400000000000000355, -9.237604307034033013, -1.753283555911559014E-16 ) ) ;
#45148=CARTESIAN_POINT ( 'NONE',  ( 0.000000000000000000, 6.928203230275506108, 4.000000000000006217 ) ) ;
#45377=CARTESIAN_POINT ( 'NONE',  ( 0.000000000000000000, 0.000000000000000000, -8.000000000000000000 ) ) ;
#45620=CARTESIAN_POINT ( 'NONE',  ( 6.400000000000000355, 4.618802153517004960, 8.000000000000000000 ) ) ;
#45664=VECTOR ( 'NONE', #6186, 1000.000000000000000 ) ;
#45774=DIRECTION ( 'NONE',  ( -1.000000000000000000, -0.000000000000000000, -0.000000000000000000 ) ) ;
#45815=CARTESIAN_POINT ( 'NONE',  ( 6.400000000000000355, 4.618802153517001408, -8.000000000000000000 ) ) ;
#45851=CARTESIAN_POINT ( 'NONE',  ( 0.4964154566687906112, 4.996589667937374912, 7.345652830558760726 ) ) ;
#46114=PRODUCT_DEFINITION ( 'UNKNOWN', '', #4097, #6401 ) ;
#46297=DIRECTION ( 'NONE',  ( 0.000000000000000000, 0.000000000000000000, -1.000000000000000000 ) ) ;
#46564=ORIENTED_EDGE ( 'NONE', *, *, #14775, .T. ) ;
#46945=SURFACE_STYLE_USAGE ( .BOTH. , #10675 ) ;
#47234=EDGE_CURVE ( 'NONE', #59875, #47585, #66380, .T. ) ;
#47447=EDGE_CURVE ( 'NONE', #16032, #20172, #5315, .T. ) ;
#47481=ORIENTED_EDGE ( 'NONE', *, *, #68780, .T. ) ;
#47490=ORIENTED_EDGE ( 'NONE', *, *, #42397, .F. ) ;
#47585=VERTEX_POINT ( 'NONE', #12201 ) ;
#47768=CARTESIAN_POINT ( 'NONE',  ( 0.1306530452038140722, -5.952467836904157927, 5.690023276062402324 ) ) ;
#47772=VERTEX_POINT ( 'NONE', #57878 ) ;
#47783=PLANE ( 'NONE',  #39555 ) ;
#47804=CARTESIAN_POINT ( 'NONE',  ( 6.400000000000000355, -9.237604307034033013, -1.753283555911559014E-16 ) ) ;
#47830=CARTESIAN_POINT ( 'NONE',  ( 6.400000000000000355, -4.618802153517011178, 8.000000000000000000 ) ) ;
#48155=DIRECTION ( 'NONE',  ( 1.000000000000000000, 0.000000000000000000, 0.000000000000000000 ) ) ;
#48341=ORIENTED_EDGE ( 'NONE', *, *, #53726, .F. ) ;
#48379=VERTEX_POINT ( 'NONE', #7379 ) ;
#48399=CARTESIAN_POINT ( 'NONE',  ( 0.000000000000000000, 0.000000000000000000, 0.000000000000000000 ) ) ;
#48519=DIRECTION ( 'NONE',  ( -0.000000000000000000, 0.8660254037844381525, 0.5000000000000008882 ) ) ;
#48534=VECTOR ( 'NONE', #28076, 1000.000000000000114 ) ;
#48596=AXIS2_PLACEMENT_3D ( 'NONE', #5190, #15057, #57965 ) ;
#48653=CARTESIAN_POINT ( 'NONE',  ( 0.4964154566688004921, -8.859816792613663949, 0.6543471694412422712 ) ) ;
#48710=ORIENTED_EDGE ( 'NONE', *, *, #66879, .F. ) ;
#48785=CARTESIAN_POINT ( 'NONE',  ( 0.000000000000000000, 0.000000000000000000, -8.000000000000000000 ) ) ;
#48789=EDGE_LOOP ( 'NONE', ( #56183, #16798, #13423, #41260, #10244 ) ) ;
#48840=FACE_OUTER_BOUND ( 'NONE', #53803, .T. ) ;
#49138=CARTESIAN_POINT ( 'NONE',  ( 0.7145311798163248573, -4.618802153517011178, 8.000000000000000000 ) ) ;
#49345=ADVANCED_FACE ( 'NONE', ( #66227 ), #51376, .T. ) ;
#49370=PLANE ( 'NONE',  #19549 ) ;
#49541=CARTESIAN_POINT ( 'NONE',  ( 0.7145311798163210826, 4.618802153517001408, -8.000000000000000000 ) ) ;
#49611=CARTESIAN_POINT ( 'NONE',  ( 4.065758146820642860E-17, 0.3912769056150356972, 8.000000000000001776 ) ) ;
#49703=ORIENTED_EDGE ( 'NONE', *, *, #16414, .T. ) ;
#49851=EDGE_CURVE ( 'NONE', #65894, #55546, #34137, .T. ) ;
#49853=EDGE_CURVE ( 'NONE', #20172, #62269, #50953, .T. ) ;
#49869=AXIS2_PLACEMENT_3D ( 'NONE', #48399, #37179, #589 ) ;
#50014=EDGE_CURVE ( 'NONE', #63967, #59875, #50900, .T. ) ;
#50056=CARTESIAN_POINT ( 'NONE',  ( 0.4964154566687932202, 8.859816792613651515, -0.6543471694412406059 ) ) ;
#50140=LINE ( 'NONE', #3675, #4595 ) ;
#50153=CARTESIAN_POINT ( 'NONE',  ( 46.39999999999999858, 0.000000000000000000, 0.000000000000000000 ) ) ;
#50530=CARTESIAN_POINT ( 'NONE',  ( 0.000000000000000000, 0.000000000000000000, 0.000000000000000000 ) ) ;
#50584=AXIS2_PLACEMENT_3D ( 'NONE', #8649, #29746, #66705 ) ;
#50649=CARTESIAN_POINT ( 'NONE',  ( 45.57199999999999562, 0.000000000000000000, 0.000000000000000000 ) ) ;
#50900=LINE ( 'NONE', #12230, #19992 ) ;
#50903=EDGE_CURVE ( 'NONE', #47585, #17657, #50140, .T. ) ;
#50953=B_SPLINE_CURVE_WITH_KNOTS ( 'NONE', 3,
 ( #48785, #980, #270, #10481, #630, #42826 ),
 .UNSPECIFIED., .F., .F.,
 ( 4, 2, 4 ),
 ( 0.02753256082175533151, 0.02987018134127081281, 0.03220780186078629065 ),
 .UNSPECIFIED. ) ;
#50971=EDGE_LOOP ( 'NONE', ( #30903, #67963, #31405 ) ) ;
#51032=AXIS2_PLACEMENT_3D ( 'NONE', #32997, #65721, #27713 ) ;
#51189=ORIENTED_EDGE ( 'NONE', *, *, #17755, .F. ) ;
#51247=VERTEX_POINT ( 'NONE', #20453 ) ;
#51376=CONICAL_SURFACE ( 'NONE', #19944, 8.000000000000000000, 1.047197551196600296 ) ;
#51498=( NAMED_UNIT ( * ) PLANE_ANGLE_UNIT ( ) SI_UNIT ( $, .RADIAN. ) );
#51671=CARTESIAN_POINT ( 'NONE',  ( 0.08224679563971432072, 7.710515798486365924, 2.644994884459109574 ) ) ;
#52000=CIRCLE ( 'NONE', #48596, 8.000000000000000000 ) ;
#52151=EDGE_LOOP ( 'NONE', ( #62887, #294 ) ) ;
#52345=LINE ( 'NONE', #58639, #10891 ) ;
#52446=EDGE_LOOP ( 'NONE', ( #68569, #9919, #25171, #47490 ) ) ;
#52541=VERTEX_POINT ( 'NONE', #2069 ) ;
#52560=PRESENTATION_STYLE_ASSIGNMENT (( #46945 ) ) ;
#52690=EDGE_CURVE ( 'NONE', #18889, #17838, #28338, .T. ) ;
#52713=FACE_OUTER_BOUND ( 'NONE', #55969, .T. ) ;
#52736=CARTESIAN_POINT ( 'NONE',  ( 46.39999999999999858, 0.000000000000000000, 0.000000000000000000 ) ) ;
#52832=CARTESIAN_POINT ( 'NONE',  ( 0.000000000000000000, 0.000000000000000000, -8.000000000000000000 ) ) ;
#52985=CIRCLE ( 'NONE', #23844, 5.000000000000000000 ) ;
#53028=CARTESIAN_POINT ( 'NONE',  ( 0.1306530452038109080, 7.903938623646869388, 2.309976723937612775 ) ) ;
#53086=AXIS2_PLACEMENT_3D ( 'NONE', #14514, #18409, #14173 ) ;
#53234=( NAMED_UNIT ( * ) SI_UNIT ( $, .STERADIAN. ) SOLID_ANGLE_UNIT ( ) );
#53261=EDGE_CURVE ( 'NONE', #56288, #47772, #52000, .T. ) ;
#53276=FACE_OUTER_BOUND ( 'NONE', #20266, .T. ) ;
#53726=EDGE_CURVE ( 'NONE', #16032, #7544, #15296, .T. ) ;
#53768=ORIENTED_EDGE ( 'NONE', *, *, #8341, .F. ) ;
#53801=ORIENTED_EDGE ( 'NONE', *, *, #40510, .F. ) ;
#53803=EDGE_LOOP ( 'NONE', ( #22232, #22889, #34439 ) ) ;
#54165=ORIENTED_EDGE ( 'NONE', *, *, #28236, .F. ) ;
#54168=AXIS2_PLACEMENT_3D ( 'NONE', #62179, #20305, #13999 ) ;
#54240=DIRECTION ( 'NONE',  ( -1.000000000000000000, -0.000000000000000000, -0.000000000000000000 ) ) ;
#54468=CARTESIAN_POINT ( 'NONE',  ( -4.856322230924655483E-17, 0.3912769056150321445, -8.000000000000000000 ) ) ;
#54552=CARTESIAN_POINT ( 'NONE',  ( 0.000000000000000000, 0.000000000000000000, 0.000000000000000000 ) ) ;
#54589=CIRCLE ( 'NONE', #33273, 4.171999999999999709 ) ;
#54910=CARTESIAN_POINT ( 'NONE',  ( 0.08224679563971232232, 6.145890662064651622, -5.355005115540898863 ) ) ;
#54976=AXIS2_PLACEMENT_3D ( 'NONE', #36360, #20868, #5032 ) ;
#55192=ORIENTED_EDGE ( 'NONE', *, *, #49851, .F. ) ;
#55322=CARTESIAN_POINT ( 'NONE',  ( -3.806566064960824935E-15, 7.321656987762869662, -3.318518101603011417 ) ) ;
#55434=ORIENTED_EDGE ( 'NONE', *, *, #10386, .F. ) ;
#55454=CONICAL_SURFACE ( 'NONE', #49869, 8.000000000000000000, 1.047197551196600296 ) ;
#55509=CARTESIAN_POINT ( 'NONE',  ( 6.400000000000000355, 4.618802153517001408, -8.000000000000000000 ) ) ;
#55546=VERTEX_POINT ( 'NONE', #62758 ) ;
#55662=EDGE_CURVE ( 'NONE', #20172, #56288, #38687, .T. ) ;
#55702=AXIS2_PLACEMENT_3D ( 'NONE', #164, #31499, #10042 ) ;
#55713=CARTESIAN_POINT ( 'NONE',  ( 0.06809871960542812630, 6.146186931204408843, 5.354491962338127742 ) ) ;
#55746=ORIENTED_EDGE ( 'NONE', *, *, #57967, .T. ) ;
#55876=DIRECTION ( 'NONE',  ( -1.000000000000000000, -0.000000000000000000, -0.000000000000000000 ) ) ;
#55969=EDGE_LOOP ( 'NONE', ( #43594, #51189, #27960, #19347, #18209 ) ) ;
#55985=CARTESIAN_POINT ( 'NONE',  ( 0.7145311798163210826, 4.618802153517001408, -8.000000000000000000 ) ) ;
#56051=CARTESIAN_POINT ( 'NONE',  ( 0.4973051450695318842, -3.866309095700718235, 8.000000000000000000 ) ) ;
#56175=CARTESIAN_POINT ( 'NONE',  ( 0.000000000000000000, -7.806255641895631925E-15, -15.99999999999998579 ) ) ;
#56183=ORIENTED_EDGE ( 'NONE', *, *, #14775, .F. ) ;
#56288=VERTEX_POINT ( 'NONE', #3075 ) ;
#56578=ORIENTED_EDGE ( 'NONE', *, *, #47447, .F. ) ;
#56719=PLANE ( 'NONE',  #43765 ) ;
#56890=ORIENTED_EDGE ( 'NONE', *, *, #13885, .F. ) ;
#56941=ORIENTED_EDGE ( 'NONE', *, *, #16414, .F. ) ;
#57516=AXIS2_PLACEMENT_3D ( 'NONE', #5294, #48519, #10562 ) ;
#57636=EDGE_LOOP ( 'NONE', ( #69521, #56578, #62015, #65377, #22482, #69056 ) ) ;
#57878=CARTESIAN_POINT ( 'NONE',  ( 0.000000000000000000, 6.928203230275506108, 4.000000000000006217 ) ) ;
#57900=ORIENTED_EDGE ( 'NONE', *, *, #53726, .T. ) ;
#57911=CIRCLE ( 'NONE', #32099, 8.000000000000000000 ) ;
#57965=DIRECTION ( 'NONE',  ( 0.000000000000000000, 0.000000000000000000, -1.000000000000000000 ) ) ;
#57967=EDGE_CURVE ( 'NONE', #65564, #56288, #25078, .T. ) ;
#58034=ORIENTED_EDGE ( 'NONE', *, *, #49853, .T. ) ;
#58161=PLANE ( 'NONE',  #54976 ) ;
#58207=EDGE_LOOP ( 'NONE', ( #64632, #55746, #7921 ) ) ;
#58472=CARTESIAN_POINT ( 'NONE',  ( 0.000000000000000000, -6.928203230275505220, -4.000000000000007105 ) ) ;
#58550=VECTOR ( 'NONE', #54240, 1000.000000000000000 ) ;
#58639=CARTESIAN_POINT ( 'NONE',  ( 0.000000000000000000, 6.123233995736766282E-16, -5.000000000000000000 ) ) ;
#58777=CARTESIAN_POINT ( 'NONE',  ( 0.000000000000000000, 0.000000000000000000, 8.000000000000000000 ) ) ;
#58831=DIRECTION ( 'NONE',  ( 1.000000000000000000, 0.000000000000000000, -0.000000000000000000 ) ) ;
#58862=ORIENTED_EDGE ( 'NONE', *, *, #34648, .T. ) ;
#58902=AXIS2_PLACEMENT_3D ( 'NONE', #36331, #31063, #60198 ) ;
#59223=CARTESIAN_POINT ( 'NONE',  ( 0.7145311798163349604, -9.237604307034033013, 2.857026868940023748E-16 ) ) ;
#59234=FACE_OUTER_BOUND ( 'NONE', #12030, .T. ) ;
#59574=DIRECTION ( 'NONE',  ( 0.000000000000000000, -0.5000000000000009992, -0.8660254037844380415 ) ) ;
#59700=CARTESIAN_POINT ( 'NONE',  ( 0.7145311798163274108, 9.237604307034018802, -2.124379920709345337E-16 ) ) ;
#59726=ORIENTED_EDGE ( 'NONE', *, *, #47447, .T. ) ;
#59875=VERTEX_POINT ( 'NONE', #39719 ) ;
#59893=CARTESIAN_POINT ( 'NONE',  ( 0.3167204509598382511, 8.479269695850865318, -1.313474075707213418 ) ) ;
#60103=CARTESIAN_POINT ( 'NONE',  ( 0.4988340113715870050, 3.871605243926952156, -8.000000000000001776 ) ) ;
#60113=ORIENTED_EDGE ( 'NONE', *, *, #20966, .T. ) ;
#60198=DIRECTION ( 'NONE',  ( -0.000000000000000000, 0.000000000000000000, 1.000000000000000000 ) ) ;
#60211=ADVANCED_FACE ( 'NONE', ( #53276 ), #37711, .T. ) ;
#60261=CARTESIAN_POINT ( 'NONE',  ( 0.06809871960542744629, 7.710219529346611367, -2.645508037661881584 ) ) ;
#60262=ORIENTED_EDGE ( 'NONE', *, *, #57967, .F. ) ;
#60343=ORIENTED_EDGE ( 'NONE', *, *, #29789, .F. ) ;
#60409=SHAPE_REPRESENTATION ( 'hex bolt gradeb_iso_ISO 4015 - M10 x 40 x 26-N', ( #66832 ), #10752 ) ;
#60641=LINE ( 'NONE', #22311, #61080 ) ;
#60664=ORIENTED_EDGE ( 'NONE', *, *, #50014, .T. ) ;
#60725=CONICAL_SURFACE ( 'NONE', #50584, 8.000000000000000000, 1.047197551196600296 ) ;
#60752=EDGE_CURVE ( 'NONE', #47772, #65564, #25779, .T. ) ;
#61053=DIRECTION ( 'NONE',  ( -1.000000000000000000, -0.000000000000000000, -0.000000000000000000 ) ) ;
#61080=VECTOR ( 'NONE', #2261, 999.9999999999998863 ) ;
#61311=CARTESIAN_POINT ( 'NONE',  ( 0.3167204509598223194, -5.377136764700217064, -6.686525924292710421 ) ) ;
#61352=LINE ( 'NONE', #24070, #35176 ) ;
#61456=DIRECTION ( 'NONE',  ( -0.000000000000000000, 0.5000000000000008882, -0.8660254037844381525 ) ) ;
#61558=DIRECTION ( 'NONE',  ( 0.000000000000000000, 0.000000000000000000, 1.000000000000000000 ) ) ;
#61656=LINE ( 'NONE', #27289, #45664 ) ;
#61856=VERTEX_POINT ( 'NONE', #19986 ) ;
#62015=ORIENTED_EDGE ( 'NONE', *, *, #18540, .F. ) ;
#62144=CARTESIAN_POINT ( 'NONE',  ( 0.000000000000000000, -6.928203230275503444, 4.000000000000010658 ) ) ;
#62179=CARTESIAN_POINT ( 'NONE',  ( 6.400000000000000355, 0.000000000000000000, 0.000000000000000000 ) ) ;
#62269=VERTEX_POINT ( 'NONE', #32818 ) ;
#62323=ORIENTED_EDGE ( 'NONE', *, *, #10386, .T. ) ;
#62327=CARTESIAN_POINT ( 'NONE',  ( 46.39999999999999858, 0.000000000000000000, 0.000000000000000000 ) ) ;
#62457=ORIENTED_EDGE ( 'NONE', *, *, #66565, .T. ) ;
#62758=CARTESIAN_POINT ( 'NONE',  ( 0.7145311798163248573, -4.618802153517011178, 8.000000000000000000 ) ) ;
#62887=ORIENTED_EDGE ( 'NONE', *, *, #52690, .T. ) ;
#62919=CARTESIAN_POINT ( 'NONE',  ( -2.954450920023000372E-15, 7.124194613927624431, 3.660532965668821248 ) ) ;
#62984=LINE ( 'NONE', #47830, #9178 ) ;
#62996=PRODUCT ( 'hex bolt gradeb_iso_ISO 4015 - M10 x 40 x 26-N', 'hex bolt gradeb_iso_ISO 4015 - M10 x 40 x 26-N', '', ( #24850 ) ) ;
#63426=CARTESIAN_POINT ( 'NONE',  ( 0.01688885742777323368, -7.321065037175435997, -3.319543390096042046 ) ) ;
#63623=MANIFOLD_SOLID_BREP ( 'HeadChamfer', #6963 ) ;
#63644=PLANE ( 'NONE',  #10852 ) ;
#63832=STYLED_ITEM ( 'NONE', ( #52560 ), #63623 ) ;
#63967=VERTEX_POINT ( 'NONE', #47804 ) ;
#64118=CARTESIAN_POINT ( 'NONE',  ( 0.000000000000000000, 0.000000000000000000, 0.000000000000000000 ) ) ;
#64122=FACE_OUTER_BOUND ( 'NONE', #17768, .T. ) ;
#64298=CARTESIAN_POINT ( 'NONE',  ( 0.08224679563971869223, -6.145890662064657839, 5.355005115540905081 ) ) ;
#64632=ORIENTED_EDGE ( 'NONE', *, *, #60752, .T. ) ;
#64675=VERTEX_POINT ( 'NONE', #45620 ) ;
#64701=CARTESIAN_POINT ( 'NONE',  ( 0.000000000000000000, 0.000000000000000000, 0.000000000000000000 ) ) ;
#64815=DIRECTION ( 'NONE',  ( 0.000000000000000000, 0.000000000000000000, -1.000000000000000000 ) ) ;
#65184=ADVANCED_FACE ( 'NONE', ( #25815, #64122 ), #58161, .T. ) ;
#65293=DIRECTION ( 'NONE',  ( 0.000000000000000000, 0.000000000000000000, -1.000000000000000000 ) ) ;
#65377=ORIENTED_EDGE ( 'NONE', *, *, #25373, .F. ) ;
#65564=VERTEX_POINT ( 'NONE', #59700 ) ;
#65721=DIRECTION ( 'NONE',  ( -1.000000000000000000, -0.000000000000000000, -0.000000000000000000 ) ) ;
#65826=DIRECTION ( 'NONE',  ( 0.000000000000000000, 0.000000000000000000, -1.000000000000000000 ) ) ;
#65849=ORIENTED_EDGE ( 'NONE', *, *, #16352, .F. ) ;
#65853=DIRECTION ( 'NONE',  ( 1.000000000000000000, 0.000000000000000000, -0.000000000000000000 ) ) ;
#65894=VERTEX_POINT ( 'NONE', #62144 ) ;
#66010=AXIS2_PLACEMENT_3D ( 'NONE', #25376, #37628, #26399 ) ;
#66059=B_SPLINE_CURVE_WITH_KNOTS ( 'NONE', 3,
 ( #12017, #12715, #39792, #54910, #8132, #23959, #28901, #18331 ),
 .UNSPECIFIED., .F., .F.,
 ( 4, 2, 2, 4 ),
 ( 0.004673709593152168724, 0.005837709341827655544, 0.007001709090503143232, 0.009329708587854116872 ),
 .UNSPECIFIED. ) ;
#66066=( GEOMETRIC_REPRESENTATION_CONTEXT ( 3 ) GLOBAL_UNCERTAINTY_ASSIGNED_CONTEXT ( ( #7882 ) ) GLOBAL_UNIT_ASSIGNED_CONTEXT ( ( #14926, #19874, #53234 ) ) REPRESENTATION_CONTEXT ( 'NONE', 'WORKASPACE' ) );
#66227=FACE_OUTER_BOUND ( 'NONE', #50971, .T. ) ;
#66380=LINE ( 'NONE', #12903, #23316 ) ;
#66565=EDGE_CURVE ( 'NONE', #4587, #61856, #6780, .T. ) ;
#66587=ORIENTED_EDGE ( 'NONE', *, *, #55662, .T. ) ;
#66606=CARTESIAN_POINT ( 'NONE',  ( 0.4964154566687647985, -4.996589667937445078, -7.345652830558659474 ) ) ;
#66705=DIRECTION ( 'NONE',  ( 0.000000000000000000, 0.000000000000000000, -1.000000000000000000 ) ) ;
#66832=AXIS2_PLACEMENT_3D ( 'NONE', #50530, #44558, #8319 ) ;
#66854=DIRECTION ( 'NONE',  ( -1.000000000000000000, -0.000000000000000000, -0.000000000000000000 ) ) ;
#66879=EDGE_CURVE ( 'NONE', #18030, #51247, #52985, .T. ) ;
#66915=CARTESIAN_POINT ( 'NONE',  ( 0.000000000000000000, 0.000000000000000000, 0.000000000000000000 ) ) ;
#67029=EDGE_LOOP ( 'NONE', ( #16463, #36289, #57900 ) ) ;
#67043=ADVANCED_FACE ( 'NONE', ( #52713 ), #47783, .F. ) ;
#67293=DIRECTION ( 'NONE',  ( 1.000000000000000000, 0.000000000000000000, 0.000000000000000000 ) ) ;
#67512=ADVANCED_FACE ( 'NONE', ( #43298 ), #38038, .T. ) ;
#67576=CARTESIAN_POINT ( 'NONE',  ( 0.000000000000000000, 0.000000000000000000, 0.000000000000000000 ) ) ;
#67809=FACE_OUTER_BOUND ( 'NONE', #18803, .T. ) ;
#67963=ORIENTED_EDGE ( 'NONE', *, *, #40510, .T. ) ;
#68041=CARTESIAN_POINT ( 'NONE',  ( 6.400000000000000355, 0.000000000000000000, 5.000000000000000000 ) ) ;
#68203=ADVANCED_FACE ( 'NONE', ( #38219 ), #55454, .T. ) ;
#68455=ORIENTED_EDGE ( 'NONE', *, *, #20966, .F. ) ;
#68548=ADVANCED_FACE ( 'NONE', ( #40308 ), #14865, .F. ) ;
#68567=DIRECTION ( 'NONE',  ( 0.000000000000000000, 0.5000000000000006661, -0.8660254037844382635 ) ) ;
#68569=ORIENTED_EDGE ( 'NONE', *, *, #22559, .F. ) ;
#68641=DIRECTION ( 'NONE',  ( -0.000000000000000000, 0.000000000000000000, 1.000000000000000000 ) ) ;
#68780=EDGE_CURVE ( 'NONE', #18030, #18889, #8133, .T. ) ;
#68921=CARTESIAN_POINT ( 'NONE',  ( 0.3157512944565082358, -3.097794232830076044, 8.000000000000000000 ) ) ;
#68969=ADVANCED_FACE ( 'NONE', ( #48840 ), #34185, .T. ) ;
#69056=ORIENTED_EDGE ( 'NONE', *, *, #53261, .F. ) ;
#69120=CARTESIAN_POINT ( 'NONE',  ( 6.400000000000000355, -9.237604307034033013, -1.753283555911559014E-16 ) ) ;
#69255=B_SPLINE_CURVE_WITH_KNOTS ( 'NONE', 3,
 ( #23682, #66606, #61311, #45125, #18396, #39853 ),
 .UNSPECIFIED., .F., .F.,
 ( 4, 2, 4 ),
 ( 2.380731631042988191E-07, 0.002336973833157624057, 0.004673709593152144438 ),
 .UNSPECIFIED. ) ;
#69521=ORIENTED_EDGE ( 'NONE', *, *, #55662, .F. ) ;
ENDSEC;
END-ISO-10303-21;
